ISO-10303-21;
HEADER;
/* Generated by software containing ST-Developer
 * from STEP Tools, Inc. (www.steptools.com) 
 */

FILE_DESCRIPTION(
/* description */ (''),
/* implementation_level */ '2;1');

FILE_NAME(
/* name */ 
'07_DIN_471_Retaining_Ring_10x1.step',
/* time_stamp */ '2026-10-22T00:21:42-07:00',
/* author */ (''),
/* organization */ (''),
/* preprocessor_version */ 'ST-DEVELOPER v20.2',
/* originating_system */ 'Autodesk Translation Framework v15.15.0.0',
/* authorisation */ '');

FILE_SCHEMA (('AUTOMOTIVE_DESIGN { 1 0 10303 214 3 1 1 }'));
ENDSEC;

DATA;
#10=MECHANICAL_DESIGN_GEOMETRIC_PRESENTATION_REPRESENTATION('',(#211),#31638);
#172=ELLIPSE('',#13107,0.678822509939079,0.48);
#173=ELLIPSE('',#13111,0.678822509939079,0.48);
#174=ELLIPSE('',#13114,0.678822509939079,0.48);
#175=ELLIPSE('',#13116,0.678822509939079,0.48);
#189=SHAPE_REPRESENTATION_RELATIONSHIP('SRR','None',#31711,#200);
#200=ADVANCED_BREP_SHAPE_REPRESENTATION('',(#222),#31633);
#211=STYLED_ITEM('',(#31844),#222);
#222=MANIFOLD_SOLID_BREP('Retaining ring',#12486);
#289=CYLINDRICAL_SURFACE('',#13113,0.48);
#290=CYLINDRICAL_SURFACE('',#13125,0.05);
#291=CYLINDRICAL_SURFACE('',#13127,0.05);
#292=CYLINDRICAL_SURFACE('',#13135,0.6);
#1392=FACE_BOUND('',#2958,.T.);
#1393=FACE_BOUND('',#2959,.T.);
#1394=FACE_BOUND('',#2969,.T.);
#1395=FACE_BOUND('',#2970,.T.);
#1649=CIRCLE('',#13115,0.48);
#1650=CIRCLE('',#13117,0.48);
#1651=CIRCLE('',#13120,0.6);
#1652=CIRCLE('',#13121,0.05);
#1653=CIRCLE('',#13122,0.05);
#1654=CIRCLE('',#13126,0.05);
#1655=CIRCLE('',#13128,0.05);
#1656=CIRCLE('',#13134,0.6);
#2204=FACE_OUTER_BOUND('',#2950,.T.);
#2205=FACE_OUTER_BOUND('',#2951,.T.);
#2206=FACE_OUTER_BOUND('',#2952,.T.);
#2207=FACE_OUTER_BOUND('',#2953,.T.);
#2208=FACE_OUTER_BOUND('',#2954,.T.);
#2209=FACE_OUTER_BOUND('',#2955,.T.);
#2210=FACE_OUTER_BOUND('',#2956,.T.);
#2211=FACE_OUTER_BOUND('',#2957,.T.);
#2212=FACE_OUTER_BOUND('',#2960,.T.);
#2213=FACE_OUTER_BOUND('',#2961,.T.);
#2214=FACE_OUTER_BOUND('',#2962,.T.);
#2215=FACE_OUTER_BOUND('',#2963,.T.);
#2216=FACE_OUTER_BOUND('',#2964,.T.);
#2217=FACE_OUTER_BOUND('',#2965,.T.);
#2218=FACE_OUTER_BOUND('',#2966,.T.);
#2219=FACE_OUTER_BOUND('',#2967,.T.);
#2220=FACE_OUTER_BOUND('',#2968,.T.);
#2221=FACE_OUTER_BOUND('',#2971,.T.);
#2950=EDGE_LOOP('',(#9921,#9922,#9923,#9924));
#2951=EDGE_LOOP('',(#9925,#9926,#9927,#9928));
#2952=EDGE_LOOP('',(#9929,#9930,#9931,#9932,#9933,#9934));
#2953=EDGE_LOOP('',(#9935,#9936,#9937,#9938));
#2954=EDGE_LOOP('',(#9939,#9940,#9941,#9942));
#2955=EDGE_LOOP('',(#9943,#9944,#9945,#9946,#9947,#9948,#9949,#9950));
#2956=EDGE_LOOP('',(#9951,#9952,#9953,#9954));
#2957=EDGE_LOOP('',(#9955,#9956,#9957,#9958,#9959,#9960,#9961,#9962,#9963,
#9964));
#2958=EDGE_LOOP('',(#9965));
#2959=EDGE_LOOP('',(#9966));
#2960=EDGE_LOOP('',(#9967,#9968,#9969,#9970));
#2961=EDGE_LOOP('',(#9971,#9972,#9973,#9974,#9975,#9976));
#2962=EDGE_LOOP('',(#9977,#9978,#9979,#9980));
#2963=EDGE_LOOP('',(#9981,#9982,#9983,#9984));
#2964=EDGE_LOOP('',(#9985,#9986,#9987,#9988));
#2965=EDGE_LOOP('',(#9989,#9990,#9991,#9992));
#2966=EDGE_LOOP('',(#9993,#9994,#9995,#9996));
#2967=EDGE_LOOP('',(#9997,#9998,#9999,#10000));
#2968=EDGE_LOOP('',(#10001,#10002,#10003,#10004,#10005,#10006,#10007,#10008,
#10009,#10010));
#2969=EDGE_LOOP('',(#10011));
#2970=EDGE_LOOP('',(#10012));
#2971=EDGE_LOOP('',(#10013,#10014,#10015,#10016));
#3554=LINE('',#25748,#4259);
#3555=LINE('',#25750,#4260);
#3556=LINE('',#25753,#4261);
#3557=LINE('',#25756,#4262);
#3558=LINE('',#25758,#4263);
#3559=LINE('',#25759,#4264);
#3560=LINE('',#25762,#4265);
#3561=LINE('',#25764,#4266);
#3562=LINE('',#25766,#4267);
#3563=LINE('',#25767,#4268);
#3564=LINE('',#25771,#4269);
#3565=LINE('',#25773,#4270);
#3566=LINE('',#25776,#4271);
#3567=LINE('',#25779,#4272);
#3568=LINE('',#25781,#4273);
#3569=LINE('',#25782,#4274);
#3570=LINE('',#25791,#4275);
#3571=LINE('',#25794,#4276);
#3572=LINE('',#25796,#4277);
#3573=LINE('',#25800,#4278);
#3574=LINE('',#25802,#4279);
#3575=LINE('',#25804,#4280);
#3576=LINE('',#25805,#4281);
#3577=LINE('',#25811,#4282);
#3578=LINE('',#25814,#4283);
#3579=LINE('',#25815,#4284);
#3580=LINE('',#25819,#4285);
#3581=LINE('',#25823,#4286);
#3582=LINE('',#25826,#4287);
#3583=LINE('',#25828,#4288);
#3584=LINE('',#25829,#4289);
#3585=LINE('',#25831,#4290);
#3586=LINE('',#25834,#4291);
#3587=LINE('',#25836,#4292);
#3588=LINE('',#25837,#4293);
#3589=LINE('',#25839,#4294);
#4259=VECTOR('',#14890,1.);
#4260=VECTOR('',#14891,1.);
#4261=VECTOR('',#14894,1.);
#4262=VECTOR('',#14897,1.);
#4263=VECTOR('',#14898,1.);
#4264=VECTOR('',#14899,1.);
#4265=VECTOR('',#14902,1.);
#4266=VECTOR('',#14903,1.);
#4267=VECTOR('',#14904,1.);
#4268=VECTOR('',#14905,1.);
#4269=VECTOR('',#14908,1.);
#4270=VECTOR('',#14909,1.);
#4271=VECTOR('',#14912,1.);
#4272=VECTOR('',#14915,1.);
#4273=VECTOR('',#14916,1.);
#4274=VECTOR('',#14917,1.);
#4275=VECTOR('',#14930,1.);
#4276=VECTOR('',#14933,1.);
#4277=VECTOR('',#14934,1.);
#4278=VECTOR('',#14937,1.);
#4279=VECTOR('',#14938,1.);
#4280=VECTOR('',#14939,1.);
#4281=VECTOR('',#14940,1.);
#4282=VECTOR('',#14947,1.);
#4283=VECTOR('',#14950,1.);
#4284=VECTOR('',#14951,1.);
#4285=VECTOR('',#14956,0.05);
#4286=VECTOR('',#14961,0.05);
#4287=VECTOR('',#14964,1.);
#4288=VECTOR('',#14965,1.);
#4289=VECTOR('',#14966,1.);
#4290=VECTOR('',#14969,1.);
#4291=VECTOR('',#14972,1.);
#4292=VECTOR('',#14973,1.);
#4293=VECTOR('',#14974,1.);
#4294=VECTOR('',#14977,1.);
#5401=VERTEX_POINT('',#25746);
#5402=VERTEX_POINT('',#25747);
#5403=VERTEX_POINT('',#25749);
#5404=VERTEX_POINT('',#25751);
#5405=VERTEX_POINT('',#25755);
#5406=VERTEX_POINT('',#25757);
#5407=VERTEX_POINT('',#25761);
#5408=VERTEX_POINT('',#25763);
#5409=VERTEX_POINT('',#25765);
#5410=VERTEX_POINT('',#25769);
#5411=VERTEX_POINT('',#25770);
#5412=VERTEX_POINT('',#25772);
#5413=VERTEX_POINT('',#25774);
#5414=VERTEX_POINT('',#25778);
#5415=VERTEX_POINT('',#25780);
#5416=VERTEX_POINT('',#25784);
#5417=VERTEX_POINT('',#25786);
#5418=VERTEX_POINT('',#25793);
#5419=VERTEX_POINT('',#25795);
#5420=VERTEX_POINT('',#25797);
#5421=VERTEX_POINT('',#25799);
#5422=VERTEX_POINT('',#25801);
#5423=VERTEX_POINT('',#25803);
#5424=VERTEX_POINT('',#25806);
#5425=VERTEX_POINT('',#25808);
#5426=VERTEX_POINT('',#25813);
#5427=VERTEX_POINT('',#25817);
#5428=VERTEX_POINT('',#25821);
#5429=VERTEX_POINT('',#25825);
#5430=VERTEX_POINT('',#25827);
#5431=VERTEX_POINT('',#25833);
#5432=VERTEX_POINT('',#25835);
#6972=EDGE_CURVE('',#5401,#5402,#3554,.T.);
#6973=EDGE_CURVE('',#5402,#5403,#3555,.T.);
#6974=EDGE_CURVE('',#5403,#5404,#172,.T.);
#6975=EDGE_CURVE('',#5404,#5401,#3556,.T.);
#6976=EDGE_CURVE('',#5402,#5405,#3557,.T.);
#6977=EDGE_CURVE('',#5406,#5405,#3558,.T.);
#6978=EDGE_CURVE('',#5403,#5406,#3559,.T.);
#6979=EDGE_CURVE('',#5401,#5407,#3560,.T.);
#6980=EDGE_CURVE('',#5407,#5408,#3561,.T.);
#6981=EDGE_CURVE('',#5409,#5408,#3562,.T.);
#6982=EDGE_CURVE('',#5405,#5409,#3563,.T.);
#6983=EDGE_CURVE('',#5410,#5411,#3564,.T.);
#6984=EDGE_CURVE('',#5411,#5412,#3565,.T.);
#6985=EDGE_CURVE('',#5412,#5413,#173,.T.);
#6986=EDGE_CURVE('',#5413,#5410,#3566,.T.);
#6987=EDGE_CURVE('',#5414,#5413,#3567,.T.);
#6988=EDGE_CURVE('',#5415,#5414,#3568,.T.);
#6989=EDGE_CURVE('',#5410,#5415,#3569,.T.);
#6990=EDGE_CURVE('',#5416,#5406,#174,.T.);
#6991=EDGE_CURVE('',#5417,#5416,#1649,.T.);
#6992=EDGE_CURVE('',#5414,#5417,#175,.T.);
#6993=EDGE_CURVE('',#5412,#5404,#1650,.T.);
#6994=EDGE_CURVE('',#5409,#5416,#3570,.T.);
#6995=EDGE_CURVE('',#5408,#5418,#3571,.T.);
#6996=EDGE_CURVE('',#5418,#5419,#3572,.T.);
#6997=EDGE_CURVE('',#5419,#5420,#1651,.T.);
#6998=EDGE_CURVE('',#5420,#5421,#3573,.T.);
#6999=EDGE_CURVE('',#5421,#5422,#3574,.T.);
#7000=EDGE_CURVE('',#5422,#5423,#3575,.T.);
#7001=EDGE_CURVE('',#5417,#5423,#3576,.T.);
#7002=EDGE_CURVE('',#5424,#5424,#1652,.T.);
#7003=EDGE_CURVE('',#5425,#5425,#1653,.T.);
#7004=EDGE_CURVE('',#5423,#5415,#3577,.T.);
#7005=EDGE_CURVE('',#5426,#5422,#3578,.T.);
#7006=EDGE_CURVE('',#5411,#5426,#3579,.T.);
#7007=EDGE_CURVE('',#5427,#5427,#1654,.T.);
#7008=EDGE_CURVE('',#5427,#5425,#3580,.T.);
#7009=EDGE_CURVE('',#5428,#5428,#1655,.T.);
#7010=EDGE_CURVE('',#5428,#5424,#3581,.T.);
#7011=EDGE_CURVE('',#5429,#5420,#3582,.T.);
#7012=EDGE_CURVE('',#5430,#5429,#3583,.T.);
#7013=EDGE_CURVE('',#5430,#5421,#3584,.T.);
#7014=EDGE_CURVE('',#5426,#5430,#3585,.T.);
#7015=EDGE_CURVE('',#5419,#5431,#3586,.T.);
#7016=EDGE_CURVE('',#5432,#5418,#3587,.T.);
#7017=EDGE_CURVE('',#5432,#5431,#3588,.T.);
#7018=EDGE_CURVE('',#5407,#5432,#3589,.T.);
#7019=EDGE_CURVE('',#5431,#5429,#1656,.T.);
#9921=ORIENTED_EDGE('',*,*,#6972,.T.);
#9922=ORIENTED_EDGE('',*,*,#6973,.T.);
#9923=ORIENTED_EDGE('',*,*,#6974,.T.);
#9924=ORIENTED_EDGE('',*,*,#6975,.T.);
#9925=ORIENTED_EDGE('',*,*,#6973,.F.);
#9926=ORIENTED_EDGE('',*,*,#6976,.T.);
#9927=ORIENTED_EDGE('',*,*,#6977,.F.);
#9928=ORIENTED_EDGE('',*,*,#6978,.F.);
#9929=ORIENTED_EDGE('',*,*,#6972,.F.);
#9930=ORIENTED_EDGE('',*,*,#6979,.T.);
#9931=ORIENTED_EDGE('',*,*,#6980,.T.);
#9932=ORIENTED_EDGE('',*,*,#6981,.F.);
#9933=ORIENTED_EDGE('',*,*,#6982,.F.);
#9934=ORIENTED_EDGE('',*,*,#6976,.F.);
#9935=ORIENTED_EDGE('',*,*,#6983,.T.);
#9936=ORIENTED_EDGE('',*,*,#6984,.T.);
#9937=ORIENTED_EDGE('',*,*,#6985,.T.);
#9938=ORIENTED_EDGE('',*,*,#6986,.T.);
#9939=ORIENTED_EDGE('',*,*,#6986,.F.);
#9940=ORIENTED_EDGE('',*,*,#6987,.F.);
#9941=ORIENTED_EDGE('',*,*,#6988,.F.);
#9942=ORIENTED_EDGE('',*,*,#6989,.F.);
#9943=ORIENTED_EDGE('',*,*,#6974,.F.);
#9944=ORIENTED_EDGE('',*,*,#6978,.T.);
#9945=ORIENTED_EDGE('',*,*,#6990,.F.);
#9946=ORIENTED_EDGE('',*,*,#6991,.F.);
#9947=ORIENTED_EDGE('',*,*,#6992,.F.);
#9948=ORIENTED_EDGE('',*,*,#6987,.T.);
#9949=ORIENTED_EDGE('',*,*,#6985,.F.);
#9950=ORIENTED_EDGE('',*,*,#6993,.T.);
#9951=ORIENTED_EDGE('',*,*,#6982,.T.);
#9952=ORIENTED_EDGE('',*,*,#6994,.T.);
#9953=ORIENTED_EDGE('',*,*,#6990,.T.);
#9954=ORIENTED_EDGE('',*,*,#6977,.T.);
#9955=ORIENTED_EDGE('',*,*,#6994,.F.);
#9956=ORIENTED_EDGE('',*,*,#6981,.T.);
#9957=ORIENTED_EDGE('',*,*,#6995,.T.);
#9958=ORIENTED_EDGE('',*,*,#6996,.T.);
#9959=ORIENTED_EDGE('',*,*,#6997,.T.);
#9960=ORIENTED_EDGE('',*,*,#6998,.T.);
#9961=ORIENTED_EDGE('',*,*,#6999,.T.);
#9962=ORIENTED_EDGE('',*,*,#7000,.T.);
#9963=ORIENTED_EDGE('',*,*,#7001,.F.);
#9964=ORIENTED_EDGE('',*,*,#6991,.T.);
#9965=ORIENTED_EDGE('',*,*,#7002,.T.);
#9966=ORIENTED_EDGE('',*,*,#7003,.T.);
#9967=ORIENTED_EDGE('',*,*,#7004,.T.);
#9968=ORIENTED_EDGE('',*,*,#6988,.T.);
#9969=ORIENTED_EDGE('',*,*,#6992,.T.);
#9970=ORIENTED_EDGE('',*,*,#7001,.T.);
#9971=ORIENTED_EDGE('',*,*,#6983,.F.);
#9972=ORIENTED_EDGE('',*,*,#6989,.T.);
#9973=ORIENTED_EDGE('',*,*,#7004,.F.);
#9974=ORIENTED_EDGE('',*,*,#7000,.F.);
#9975=ORIENTED_EDGE('',*,*,#7005,.F.);
#9976=ORIENTED_EDGE('',*,*,#7006,.F.);
#9977=ORIENTED_EDGE('',*,*,#7007,.F.);
#9978=ORIENTED_EDGE('',*,*,#7008,.T.);
#9979=ORIENTED_EDGE('',*,*,#7003,.F.);
#9980=ORIENTED_EDGE('',*,*,#7008,.F.);
#9981=ORIENTED_EDGE('',*,*,#7009,.F.);
#9982=ORIENTED_EDGE('',*,*,#7010,.T.);
#9983=ORIENTED_EDGE('',*,*,#7002,.F.);
#9984=ORIENTED_EDGE('',*,*,#7010,.F.);
#9985=ORIENTED_EDGE('',*,*,#7011,.F.);
#9986=ORIENTED_EDGE('',*,*,#7012,.F.);
#9987=ORIENTED_EDGE('',*,*,#7013,.T.);
#9988=ORIENTED_EDGE('',*,*,#6998,.F.);
#9989=ORIENTED_EDGE('',*,*,#7014,.F.);
#9990=ORIENTED_EDGE('',*,*,#7005,.T.);
#9991=ORIENTED_EDGE('',*,*,#6999,.F.);
#9992=ORIENTED_EDGE('',*,*,#7013,.F.);
#9993=ORIENTED_EDGE('',*,*,#7015,.F.);
#9994=ORIENTED_EDGE('',*,*,#6996,.F.);
#9995=ORIENTED_EDGE('',*,*,#7016,.F.);
#9996=ORIENTED_EDGE('',*,*,#7017,.T.);
#9997=ORIENTED_EDGE('',*,*,#7018,.T.);
#9998=ORIENTED_EDGE('',*,*,#7016,.T.);
#9999=ORIENTED_EDGE('',*,*,#6995,.F.);
#10000=ORIENTED_EDGE('',*,*,#6980,.F.);
#10001=ORIENTED_EDGE('',*,*,#6975,.F.);
#10002=ORIENTED_EDGE('',*,*,#6993,.F.);
#10003=ORIENTED_EDGE('',*,*,#6984,.F.);
#10004=ORIENTED_EDGE('',*,*,#7006,.T.);
#10005=ORIENTED_EDGE('',*,*,#7014,.T.);
#10006=ORIENTED_EDGE('',*,*,#7012,.T.);
#10007=ORIENTED_EDGE('',*,*,#7019,.F.);
#10008=ORIENTED_EDGE('',*,*,#7017,.F.);
#10009=ORIENTED_EDGE('',*,*,#7018,.F.);
#10010=ORIENTED_EDGE('',*,*,#6979,.F.);
#10011=ORIENTED_EDGE('',*,*,#7007,.T.);
#10012=ORIENTED_EDGE('',*,*,#7009,.T.);
#10013=ORIENTED_EDGE('',*,*,#7011,.T.);
#10014=ORIENTED_EDGE('',*,*,#6997,.F.);
#10015=ORIENTED_EDGE('',*,*,#7015,.T.);
#10016=ORIENTED_EDGE('',*,*,#7019,.T.);
#11583=PLANE('',#13106);
#11584=PLANE('',#13108);
#11585=PLANE('',#13109);
#11586=PLANE('',#13110);
#11587=PLANE('',#13112);
#11588=PLANE('',#13118);
#11589=PLANE('',#13119);
#11590=PLANE('',#13123);
#11591=PLANE('',#13124);
#11592=PLANE('',#13129);
#11593=PLANE('',#13130);
#11594=PLANE('',#13131);
#11595=PLANE('',#13132);
#11596=PLANE('',#13133);
#12171=ADVANCED_FACE('',(#2204),#11583,.T.);
#12172=ADVANCED_FACE('',(#2205),#11584,.F.);
#12173=ADVANCED_FACE('',(#2206),#11585,.T.);
#12174=ADVANCED_FACE('',(#2207),#11586,.T.);
#12175=ADVANCED_FACE('',(#2208),#11587,.F.);
#12176=ADVANCED_FACE('',(#2209),#289,.F.);
#12177=ADVANCED_FACE('',(#2210),#11588,.T.);
#12178=ADVANCED_FACE('',(#2211,#1392,#1393),#11589,.T.);
#12179=ADVANCED_FACE('',(#2212),#11590,.T.);
#12180=ADVANCED_FACE('',(#2213),#11591,.T.);
#12181=ADVANCED_FACE('',(#2214),#290,.F.);
#12182=ADVANCED_FACE('',(#2215),#291,.F.);
#12183=ADVANCED_FACE('',(#2216),#11592,.T.);
#12184=ADVANCED_FACE('',(#2217),#11593,.T.);
#12185=ADVANCED_FACE('',(#2218),#11594,.T.);
#12186=ADVANCED_FACE('',(#2219),#11595,.T.);
#12187=ADVANCED_FACE('',(#2220,#1394,#1395),#11596,.F.);
#12188=ADVANCED_FACE('',(#2221),#292,.T.);
#12486=CLOSED_SHELL('',(#12171,#12172,#12173,#12174,#12175,#12176,#12177,
#12178,#12179,#12180,#12181,#12182,#12183,#12184,#12185,#12186,#12187,#12188));
#13105=AXIS2_PLACEMENT_3D('',#25744,#14886,#14887);
#13106=AXIS2_PLACEMENT_3D('',#25745,#14888,#14889);
#13107=AXIS2_PLACEMENT_3D('',#25752,#14892,#14893);
#13108=AXIS2_PLACEMENT_3D('',#25754,#14895,#14896);
#13109=AXIS2_PLACEMENT_3D('',#25760,#14900,#14901);
#13110=AXIS2_PLACEMENT_3D('',#25768,#14906,#14907);
#13111=AXIS2_PLACEMENT_3D('',#25775,#14910,#14911);
#13112=AXIS2_PLACEMENT_3D('',#25777,#14913,#14914);
#13113=AXIS2_PLACEMENT_3D('',#25783,#14918,#14919);
#13114=AXIS2_PLACEMENT_3D('',#25785,#14920,#14921);
#13115=AXIS2_PLACEMENT_3D('',#25787,#14922,#14923);
#13116=AXIS2_PLACEMENT_3D('',#25788,#14924,#14925);
#13117=AXIS2_PLACEMENT_3D('',#25789,#14926,#14927);
#13118=AXIS2_PLACEMENT_3D('',#25790,#14928,#14929);
#13119=AXIS2_PLACEMENT_3D('',#25792,#14931,#14932);
#13120=AXIS2_PLACEMENT_3D('',#25798,#14935,#14936);
#13121=AXIS2_PLACEMENT_3D('',#25807,#14941,#14942);
#13122=AXIS2_PLACEMENT_3D('',#25809,#14943,#14944);
#13123=AXIS2_PLACEMENT_3D('',#25810,#14945,#14946);
#13124=AXIS2_PLACEMENT_3D('',#25812,#14948,#14949);
#13125=AXIS2_PLACEMENT_3D('',#25816,#14952,#14953);
#13126=AXIS2_PLACEMENT_3D('',#25818,#14954,#14955);
#13127=AXIS2_PLACEMENT_3D('',#25820,#14957,#14958);
#13128=AXIS2_PLACEMENT_3D('',#25822,#14959,#14960);
#13129=AXIS2_PLACEMENT_3D('',#25824,#14962,#14963);
#13130=AXIS2_PLACEMENT_3D('',#25830,#14967,#14968);
#13131=AXIS2_PLACEMENT_3D('',#25832,#14970,#14971);
#13132=AXIS2_PLACEMENT_3D('',#25838,#14975,#14976);
#13133=AXIS2_PLACEMENT_3D('',#25840,#14978,#14979);
#13134=AXIS2_PLACEMENT_3D('',#25841,#14980,#14981);
#13135=AXIS2_PLACEMENT_3D('',#25842,#14982,#14983);
#14886=DIRECTION('axis',(0.,0.,1.));
#14887=DIRECTION('refdir',(1.,0.,0.));
#14888=DIRECTION('center_axis',(0.,-0.70710678118654,-0.707106781186555));
#14889=DIRECTION('ref_axis',(-1.,0.,0.));
#14890=DIRECTION('',(0.,-0.707106781186555,0.70710678118654));
#14891=DIRECTION('',(-1.,0.,0.));
#14892=DIRECTION('center_axis',(0.,0.70710678118654,0.707106781186555));
#14893=DIRECTION('ref_axis',(0.,0.707106781186555,-0.70710678118654));
#14894=DIRECTION('',(1.,0.,0.));
#14895=DIRECTION('center_axis',(0.,1.,0.));
#14896=DIRECTION('ref_axis',(-1.,0.,0.));
#14897=DIRECTION('',(0.,0.,1.));
#14898=DIRECTION('',(1.,0.,0.));
#14899=DIRECTION('',(0.,0.,1.));
#14900=DIRECTION('center_axis',(1.,0.,0.));
#14901=DIRECTION('ref_axis',(0.,1.,0.));
#14902=DIRECTION('',(0.,1.,0.));
#14903=DIRECTION('',(0.,0.,1.));
#14904=DIRECTION('',(0.,1.,0.));
#14905=DIRECTION('',(0.,0.707106781186555,0.70710678118654));
#14906=DIRECTION('center_axis',(0.,0.70710678118654,-0.707106781186555));
#14907=DIRECTION('ref_axis',(-1.,0.,0.));
#14908=DIRECTION('',(0.,-0.707106781186555,-0.70710678118654));
#14909=DIRECTION('',(-1.,0.,0.));
#14910=DIRECTION('center_axis',(0.,-0.70710678118654,0.707106781186555));
#14911=DIRECTION('ref_axis',(0.,0.707106781186555,0.70710678118654));
#14912=DIRECTION('',(1.,0.,0.));
#14913=DIRECTION('center_axis',(0.,-1.,0.));
#14914=DIRECTION('ref_axis',(1.,0.,0.));
#14915=DIRECTION('',(0.,0.,-1.));
#14916=DIRECTION('',(-1.,0.,0.));
#14917=DIRECTION('',(0.,0.,1.));
#14918=DIRECTION('center_axis',(0.,0.,1.));
#14919=DIRECTION('ref_axis',(-1.,1.22464679914735E-16,0.));
#14920=DIRECTION('center_axis',(0.,0.70710678118654,-0.707106781186555));
#14921=DIRECTION('ref_axis',(0.,0.707106781186555,0.70710678118654));
#14922=DIRECTION('center_axis',(0.,0.,-1.));
#14923=DIRECTION('ref_axis',(1.,0.,0.));
#14924=DIRECTION('center_axis',(0.,-0.70710678118654,-0.707106781186555));
#14925=DIRECTION('ref_axis',(0.,0.707106781186555,-0.70710678118654));
#14926=DIRECTION('center_axis',(0.,0.,-1.));
#14927=DIRECTION('ref_axis',(1.,0.,0.));
#14928=DIRECTION('center_axis',(0.,-0.70710678118654,0.707106781186555));
#14929=DIRECTION('ref_axis',(1.,0.,0.));
#14930=DIRECTION('',(-1.,0.,0.));
#14931=DIRECTION('center_axis',(0.,0.,1.));
#14932=DIRECTION('ref_axis',(1.,0.,0.));
#14933=DIRECTION('',(-1.,0.,0.));
#14934=DIRECTION('',(0.,-1.,0.));
#14935=DIRECTION('center_axis',(0.,0.,1.));
#14936=DIRECTION('ref_axis',(1.,0.,0.));
#14937=DIRECTION('',(0.,-1.,0.));
#14938=DIRECTION('',(1.,0.,0.));
#14939=DIRECTION('',(0.,1.,0.));
#14940=DIRECTION('',(1.,0.,0.));
#14941=DIRECTION('center_axis',(0.,0.,-1.));
#14942=DIRECTION('ref_axis',(1.,0.,0.));
#14943=DIRECTION('center_axis',(0.,0.,-1.));
#14944=DIRECTION('ref_axis',(1.,0.,0.));
#14945=DIRECTION('center_axis',(0.,0.70710678118654,0.707106781186555));
#14946=DIRECTION('ref_axis',(1.,0.,0.));
#14947=DIRECTION('',(0.,0.707106781186555,-0.70710678118654));
#14948=DIRECTION('center_axis',(1.,0.,0.));
#14949=DIRECTION('ref_axis',(0.,1.,0.));
#14950=DIRECTION('',(0.,0.,1.));
#14951=DIRECTION('',(0.,-1.,0.));
#14952=DIRECTION('center_axis',(0.,0.,1.));
#14953=DIRECTION('ref_axis',(1.,0.,0.));
#14954=DIRECTION('center_axis',(0.,0.,1.));
#14955=DIRECTION('ref_axis',(1.,0.,0.));
#14956=DIRECTION('',(0.,0.,1.));
#14957=DIRECTION('center_axis',(0.,0.,1.));
#14958=DIRECTION('ref_axis',(1.,0.,0.));
#14959=DIRECTION('center_axis',(0.,0.,1.));
#14960=DIRECTION('ref_axis',(1.,0.,0.));
#14961=DIRECTION('',(0.,0.,1.));
#14962=DIRECTION('center_axis',(-1.,0.,0.));
#14963=DIRECTION('ref_axis',(0.,-1.,0.));
#14964=DIRECTION('',(0.,0.,1.));
#14965=DIRECTION('',(0.,1.,0.));
#14966=DIRECTION('',(0.,0.,1.));
#14967=DIRECTION('center_axis',(0.,-1.,0.));
#14968=DIRECTION('ref_axis',(1.,0.,0.));
#14969=DIRECTION('',(-1.,0.,0.));
#14970=DIRECTION('center_axis',(-1.,0.,0.));
#14971=DIRECTION('ref_axis',(0.,-1.,0.));
#14972=DIRECTION('',(0.,0.,-1.));
#14973=DIRECTION('',(0.,0.,1.));
#14974=DIRECTION('',(0.,-1.,0.));
#14975=DIRECTION('center_axis',(0.,1.,0.));
#14976=DIRECTION('ref_axis',(-1.,0.,0.));
#14977=DIRECTION('',(-1.,0.,0.));
#14978=DIRECTION('center_axis',(0.,0.,1.));
#14979=DIRECTION('ref_axis',(1.,0.,0.));
#14980=DIRECTION('center_axis',(0.,0.,1.));
#14981=DIRECTION('ref_axis',(1.,0.,0.));
#14982=DIRECTION('center_axis',(0.,0.,1.));
#14983=DIRECTION('ref_axis',(-1.,-1.22464679914735E-16,0.));
#25744=CARTESIAN_POINT('',(0.,0.,0.));
#25745=CARTESIAN_POINT('Origin',(0.35,0.16,5.76));
#25746=CARTESIAN_POINT('',(0.79,0.17,5.75));
#25747=CARTESIAN_POINT('',(0.79,0.15,5.77));
#25748=CARTESIAN_POINT('',(0.79,0.16,5.76));
#25749=CARTESIAN_POINT('',(0.45596052460712,0.15,5.77));
#25750=CARTESIAN_POINT('',(0.35,0.15,5.77));
#25751=CARTESIAN_POINT('',(0.448887513749269,0.17,5.75));
#25752=CARTESIAN_POINT('Origin',(0.,0.,5.92));
#25753=CARTESIAN_POINT('',(0.35,0.17,5.75));
#25754=CARTESIAN_POINT('Origin',(0.7,0.15,5.75));
#25755=CARTESIAN_POINT('',(0.79,0.15,5.83));
#25756=CARTESIAN_POINT('',(0.79,0.15,5.75));
#25757=CARTESIAN_POINT('',(0.45596052460712,0.15,5.83));
#25758=CARTESIAN_POINT('',(0.35,0.15,5.83));
#25759=CARTESIAN_POINT('',(0.45596052460712,0.15,5.75));
#25760=CARTESIAN_POINT('Origin',(0.79,0.15,5.75));
#25761=CARTESIAN_POINT('',(0.79,0.4,5.75));
#25762=CARTESIAN_POINT('',(0.79,0.15,5.75));
#25763=CARTESIAN_POINT('',(0.79,0.4,5.85));
#25764=CARTESIAN_POINT('',(0.79,0.4,5.75));
#25765=CARTESIAN_POINT('',(0.79,0.17,5.85));
#25766=CARTESIAN_POINT('',(0.79,0.15,5.85));
#25767=CARTESIAN_POINT('',(0.79,0.135,5.815));
#25768=CARTESIAN_POINT('Origin',(0.19,-0.16,5.76));
#25769=CARTESIAN_POINT('',(0.79,-0.15,5.77));
#25770=CARTESIAN_POINT('',(0.79,-0.17,5.75));
#25771=CARTESIAN_POINT('',(0.79,-0.222500000000001,5.6975));
#25772=CARTESIAN_POINT('',(0.448887513749269,-0.17,5.75));
#25773=CARTESIAN_POINT('',(0.19,-0.17,5.75));
#25774=CARTESIAN_POINT('',(0.45596052460712,-0.15,5.77));
#25775=CARTESIAN_POINT('Origin',(0.,0.,5.92));
#25776=CARTESIAN_POINT('',(0.19,-0.15,5.77));
#25777=CARTESIAN_POINT('Origin',(0.38,-0.15,5.75));
#25778=CARTESIAN_POINT('',(0.45596052460712,-0.15,5.83));
#25779=CARTESIAN_POINT('',(0.45596052460712,-0.15,5.75));
#25780=CARTESIAN_POINT('',(0.79,-0.15,5.83));
#25781=CARTESIAN_POINT('',(0.19,-0.15,5.83));
#25782=CARTESIAN_POINT('',(0.79,-0.15,5.75));
#25783=CARTESIAN_POINT('Origin',(0.,0.,5.75));
#25784=CARTESIAN_POINT('',(0.448887513749269,0.17,5.85));
#25785=CARTESIAN_POINT('Origin',(0.,0.,5.68));
#25786=CARTESIAN_POINT('',(0.448887513749269,-0.17,5.85));
#25787=CARTESIAN_POINT('Origin',(0.,0.,5.85));
#25788=CARTESIAN_POINT('Origin',(0.,0.,5.68));
#25789=CARTESIAN_POINT('Origin',(0.,0.,5.75));
#25790=CARTESIAN_POINT('Origin',(0.35,0.16,5.84));
#25791=CARTESIAN_POINT('',(0.35,0.17,5.85));
#25792=CARTESIAN_POINT('Origin',(0.,0.,5.85));
#25793=CARTESIAN_POINT('',(0.55,0.4,5.85));
#25794=CARTESIAN_POINT('',(0.79,0.4,5.85));
#25795=CARTESIAN_POINT('',(0.55,0.239791576165636,5.85));
#25796=CARTESIAN_POINT('',(0.55,0.4,5.85));
#25797=CARTESIAN_POINT('',(0.55,-0.239791576165636,5.85));
#25798=CARTESIAN_POINT('Origin',(0.,0.,5.85));
#25799=CARTESIAN_POINT('',(0.55,-0.4,5.85));
#25800=CARTESIAN_POINT('',(0.55,-0.4,5.85));
#25801=CARTESIAN_POINT('',(0.79,-0.4,5.85));
#25802=CARTESIAN_POINT('',(0.79,-0.4,5.85));
#25803=CARTESIAN_POINT('',(0.79,-0.17,5.85));
#25804=CARTESIAN_POINT('',(0.79,-0.15,5.85));
#25805=CARTESIAN_POINT('',(0.19,-0.17,5.85));
#25806=CARTESIAN_POINT('',(0.65,-0.275,5.85));
#25807=CARTESIAN_POINT('Origin',(0.7,-0.275,5.85));
#25808=CARTESIAN_POINT('',(0.65,0.275,5.85));
#25809=CARTESIAN_POINT('Origin',(0.7,0.275,5.85));
#25810=CARTESIAN_POINT('Origin',(0.19,-0.16,5.84));
#25811=CARTESIAN_POINT('',(0.79,-0.197500000000001,5.8775));
#25812=CARTESIAN_POINT('Origin',(0.79,-0.4,5.75));
#25813=CARTESIAN_POINT('',(0.79,-0.4,5.75));
#25814=CARTESIAN_POINT('',(0.79,-0.4,5.75));
#25815=CARTESIAN_POINT('',(0.79,-0.15,5.75));
#25816=CARTESIAN_POINT('Origin',(0.7,0.275,5.75));
#25817=CARTESIAN_POINT('',(0.65,0.275,5.75));
#25818=CARTESIAN_POINT('Origin',(0.7,0.275,5.75));
#25819=CARTESIAN_POINT('',(0.65,0.275,5.75));
#25820=CARTESIAN_POINT('Origin',(0.7,-0.275,5.75));
#25821=CARTESIAN_POINT('',(0.65,-0.275,5.75));
#25822=CARTESIAN_POINT('Origin',(0.7,-0.275,5.75));
#25823=CARTESIAN_POINT('',(0.65,-0.275,5.75));
#25824=CARTESIAN_POINT('Origin',(0.55,-0.15,5.75));
#25825=CARTESIAN_POINT('',(0.55,-0.239791576165636,5.75));
#25826=CARTESIAN_POINT('',(0.55,-0.239791576165636,5.75));
#25827=CARTESIAN_POINT('',(0.55,-0.4,5.75));
#25828=CARTESIAN_POINT('',(0.55,-0.4,5.75));
#25829=CARTESIAN_POINT('',(0.55,-0.4,5.75));
#25830=CARTESIAN_POINT('Origin',(0.55,-0.4,5.75));
#25831=CARTESIAN_POINT('',(0.79,-0.4,5.75));
#25832=CARTESIAN_POINT('Origin',(0.55,0.4,5.75));
#25833=CARTESIAN_POINT('',(0.55,0.239791576165636,5.75));
#25834=CARTESIAN_POINT('',(0.55,0.239791576165636,5.75));
#25835=CARTESIAN_POINT('',(0.55,0.4,5.75));
#25836=CARTESIAN_POINT('',(0.55,0.4,5.75));
#25837=CARTESIAN_POINT('',(0.55,0.4,5.75));
#25838=CARTESIAN_POINT('Origin',(0.79,0.4,5.75));
#25839=CARTESIAN_POINT('',(0.79,0.4,5.75));
#25840=CARTESIAN_POINT('Origin',(0.,0.,5.75));
#25841=CARTESIAN_POINT('Origin',(0.,0.,5.75));
#25842=CARTESIAN_POINT('Origin',(0.,0.,5.75));
#31620=UNCERTAINTY_MEASURE_WITH_UNIT(LENGTH_MEASURE(0.001),#31639,
'DISTANCE_ACCURACY_VALUE',
'Maximum model space distance between geometric entities at asserted c
onnectivities');
#31625=UNCERTAINTY_MEASURE_WITH_UNIT(LENGTH_MEASURE(0.001),#31639,
'DISTANCE_ACCURACY_VALUE',
'Maximum model space distance between geometric entities at asserted c
onnectivities');
#31633=(
GEOMETRIC_REPRESENTATION_CONTEXT(3)
GLOBAL_UNCERTAINTY_ASSIGNED_CONTEXT((#31620))
GLOBAL_UNIT_ASSIGNED_CONTEXT((#31639,#31641,#31642))
REPRESENTATION_CONTEXT('','3D')
);
#31638=(
GEOMETRIC_REPRESENTATION_CONTEXT(3)
GLOBAL_UNCERTAINTY_ASSIGNED_CONTEXT((#31625))
GLOBAL_UNIT_ASSIGNED_CONTEXT((#31639,#31641,#31642))
REPRESENTATION_CONTEXT('','3D')
);
#31639=(
LENGTH_UNIT()
NAMED_UNIT(*)
SI_UNIT(.CENTI.,.METRE.)
);
#31641=(
NAMED_UNIT(*)
PLANE_ANGLE_UNIT()
SI_UNIT($,.RADIAN.)
);
#31642=(
NAMED_UNIT(*)
SI_UNIT($,.STERADIAN.)
SOLID_ANGLE_UNIT()
);
#31650=SHAPE_DEFINITION_REPRESENTATION(#31662,#31711);
#31662=PRODUCT_DEFINITION_SHAPE('',$,#31724);
#31711=SHAPE_REPRESENTATION('',(#13105),#31633);
#31716=PRODUCT_DEFINITION_CONTEXT('part definition',#31754,'design');
#31724=PRODUCT_DEFINITION('2026-10-22-02-42-21-963',
'07_DIN_471_Retaining_Ring_10x1',#31736,#31716);
#31736=PRODUCT_DEFINITION_FORMATION('',$,#31763);
#31754=APPLICATION_CONTEXT(
'Core Data for Automotive Mechanical Design Process');
#31755=PRODUCT_CONTEXT('part definition',#31754,'mechanical');
#31763=PRODUCT('2026-10-22-02-42-21-963',
'07_DIN_471_Retaining_Ring_10x1',$,(#31755));
#31838=COLOUR_RGB('Off White',0.89,0.88,0.83);
#31839=FILL_AREA_STYLE_COLOUR('',#31838);
#31840=FILL_AREA_STYLE('',(#31839));
#31841=SURFACE_STYLE_FILL_AREA(#31840);
#31842=SURFACE_SIDE_STYLE('',(#31841));
#31843=SURFACE_STYLE_USAGE(.BOTH.,#31842);
#31844=PRESENTATION_STYLE_ASSIGNMENT((#31843));
ENDSEC;
END-ISO-10303-21;
